ISO-10303-21;
HEADER;
FILE_DESCRIPTION (('STEP AP214'),
    '1' );
FILE_NAME ('Bolt3.step',
    '2026-10-28T16:39:03',
    ( '' ),
    ( '' ),
    'SwSTEP 2.0',
    'SolidWorks 2024',
    '' );
FILE_SCHEMA (( 'AUTOMOTIVE_DESIGN' ));
ENDSEC;

DATA;
#6=DIRECTION ( 'NONE',  ( 1.000000000000000000, 0.000000000000000000, 0.000000000000000000 ) ) ;
#24=ADVANCED_FACE ( 'NONE', ( #907 ), #1513, .T. ) ;
#46=DIRECTION ( 'NONE',  ( 0.7071067811865502373, 0.000000000000000000, 0.7071067811865447972 ) ) ;
#90=DIRECTION ( 'NONE',  ( -0.000000000000000000, -0.000000000000000000, -1.000000000000000000 ) ) ;
#127=EDGE_CURVE ( 'NONE', #5728, #5686, #5812, .T. ) ;
#176=CARTESIAN_POINT ( 'NONE',  ( -9.999999999999896971, 1.377727649040766078E-15, 0.000000000000000000 ) ) ;
#206=CARTESIAN_POINT ( 'NONE',  ( 12.50000000000000000, 0.000000000000000000, 2.500000000000085265 ) ) ;
#259=SHAPE_REPRESENTATION_RELATIONSHIP ( 'NONE' , 'NONE' ,  #6910, #2683 ) ;
#260=VERTEX_POINT ( 'NONE', #6838 ) ;
#387=VERTEX_POINT ( 'NONE', #176 ) ;
#389=VERTEX_POINT ( 'NONE', #5722 ) ;
#394=CARTESIAN_POINT ( 'NONE',  ( 0.000000000000000000, 0.000000000000000000, 92.50000000000000000 ) ) ;
#411=FACE_OUTER_BOUND ( 'NONE', #2301, .T. ) ;
#440=ORIENTED_EDGE ( 'NONE', *, *, #5822, .T. ) ;
#452=AXIS2_PLACEMENT_3D ( 'NONE', #4358, #6815, #1317 ) ;
#492=CIRCLE ( 'NONE', #3934, 12.50000000000000000 ) ;
#513=AXIS2_PLACEMENT_3D ( 'NONE', #5625, #3065, #6 ) ;
#514=ORIENTED_EDGE ( 'NONE', *, *, #7045, .F. ) ;
#543=CARTESIAN_POINT ( 'NONE',  ( -12.50000000000000000, 0.000000000000000000, 90.00000000000000000 ) ) ;
#545=EDGE_CURVE ( 'NONE', #3577, #4697, #5265, .T. ) ;
#644=ADVANCED_FACE ( 'NONE', ( #4987 ), #6792, .T. ) ;
#677=FACE_OUTER_BOUND ( 'NONE', #1313, .T. ) ;
#706=ORIENTED_EDGE ( 'NONE', *, *, #2407, .F. ) ;
#735=EDGE_CURVE ( 'NONE', #389, #387, #1592, .T. ) ;
#800=CARTESIAN_POINT ( 'NONE',  ( -12.50000000000000355, 1.530808498934191916E-15, 92.50000000000000000 ) ) ;
#884=DIRECTION ( 'NONE',  ( -0.000000000000000000, -0.000000000000000000, -1.000000000000000000 ) ) ;
#907=FACE_OUTER_BOUND ( 'NONE', #4552, .T. ) ;
#918=ORIENTED_EDGE ( 'NONE', *, *, #1103, .T. ) ;
#937=UNCERTAINTY_MEASURE_WITH_UNIT (LENGTH_MEASURE( 1.000000000000000082E-05 ), #5795, 'distance_accuracy_value', 'NONE');
#969=CARTESIAN_POINT ( 'NONE',  ( 0.000000000000000000, 0.000000000000000000, 92.50000000000000000 ) ) ;
#1012=CARTESIAN_POINT ( 'NONE',  ( -17.50000000000000355, 0.000000000000000000, 90.00000000000000000 ) ) ;
#1013=DIRECTION ( 'NONE',  ( -0.000000000000000000, -0.000000000000000000, -1.000000000000000000 ) ) ;
#1103=EDGE_CURVE ( 'NONE', #4697, #4272, #6184, .T. ) ;
#1127=CYLINDRICAL_SURFACE ( 'NONE', #4597, 17.50000000000000355 ) ;
#1133=CARTESIAN_POINT ( 'NONE',  ( 0.000000000000000000, 0.000000000000000000, 92.50000000000000000 ) ) ;
#1153=DIRECTION ( 'NONE',  ( 0.000000000000000000, 0.000000000000000000, 1.000000000000000000 ) ) ;
#1179=CARTESIAN_POINT ( 'NONE',  ( -17.50000000000000355, 0.000000000000000000, 97.50000000000000000 ) ) ;
#1260=FACE_BOUND ( 'NONE', #2868, .T. ) ;
#1280=ORIENTED_EDGE ( 'NONE', *, *, #4577, .T. ) ;
#1284=ORIENTED_EDGE ( 'NONE', *, *, #545, .T. ) ;
#1298=PLANE ( 'NONE',  #4390 ) ;
#1313=EDGE_LOOP ( 'NONE', ( #6943, #440, #6860, #4930 ) ) ;
#1314=CARTESIAN_POINT ( 'NONE',  ( -12.50000000000000355, 1.836970198721030378E-15, 97.50000000000000000 ) ) ;
#1317=DIRECTION ( 'NONE',  ( 1.000000000000000000, 0.000000000000000000, 0.000000000000000000 ) ) ;
#1411=FACE_OUTER_BOUND ( 'NONE', #3002, .T. ) ;
#1453=DIRECTION ( 'NONE',  ( 0.000000000000000000, 0.000000000000000000, 1.000000000000000000 ) ) ;
#1461=AXIS2_PLACEMENT_3D ( 'NONE', #800, #4329, #3748 ) ;
#1498=CARTESIAN_POINT ( 'NONE',  ( 17.50000000000000355, 2.143131898507868643E-15, 90.00000000000000000 ) ) ;
#1513=CYLINDRICAL_SURFACE ( 'NONE', #7735, 17.50000000000000355 ) ;
#1516=APPLICATION_CONTEXT ( 'automotive_design' ) ;
#1532=DIRECTION ( 'NONE',  ( 1.000000000000000000, 0.000000000000000000, 0.000000000000000000 ) ) ;
#1538=PRODUCT_DEFINITION ( 'UNKNOWN', '', #6554, #3353 ) ;
#1592=CIRCLE ( 'NONE', #1849, 9.999999999999896971 ) ;
#1661=SHAPE_DEFINITION_REPRESENTATION ( #6491, #6910 ) ;
#1664=CARTESIAN_POINT ( 'NONE',  ( -12.50000000000000000, 1.530808498934191521E-15, 2.500000000000085265 ) ) ;
#1833=FACE_OUTER_BOUND ( 'NONE', #3227, .T. ) ;
#1849=AXIS2_PLACEMENT_3D ( 'NONE', #6710, #5017, #6116 ) ;
#1869=ORIENTED_EDGE ( 'NONE', *, *, #735, .T. ) ;
#1898=ADVANCED_FACE ( 'NONE', ( #1260, #4301 ), #1298, .F. ) ;
#1944=EDGE_LOOP ( 'NONE', ( #706, #7871, #5535, #5122 ) ) ;
#1970=AXIS2_PLACEMENT_3D ( 'NONE', #5204, #884, #3336 ) ;
#1978=CARTESIAN_POINT ( 'NONE',  ( 0.000000000000000000, 0.000000000000000000, 97.50000000000000000 ) ) ;
#1988=ORIENTED_EDGE ( 'NONE', *, *, #2635, .T. ) ;
#2026=CIRCLE ( 'NONE', #3069, 12.50000000000000000 ) ;
#2031=ORIENTED_EDGE ( 'NONE', *, *, #127, .T. ) ;
#2083=DIRECTION ( 'NONE',  ( 1.000000000000000000, 0.000000000000000000, 0.000000000000000000 ) ) ;
#2087=CARTESIAN_POINT ( 'NONE',  ( 0.000000000000000000, 0.000000000000000000, 97.50000000000000000 ) ) ;
#2088=DIRECTION ( 'NONE',  ( -0.000000000000000000, -0.000000000000000000, 1.000000000000000000 ) ) ;
#2102=VECTOR ( 'NONE', #4565, 1000.000000000000000 ) ;
#2104=AXIS2_PLACEMENT_3D ( 'NONE', #7494, #6733, #4962 ) ;
#2136=ADVANCED_FACE ( 'NONE', ( #2262 ), #2781, .F. ) ;
#2204=EDGE_LOOP ( 'NONE', ( #7614, #2465 ) ) ;
#2230=AXIS2_PLACEMENT_3D ( 'NONE', #4191, #7254, #4670 ) ;
#2246=AXIS2_PLACEMENT_3D ( 'NONE', #6829, #90, #4300 ) ;
#2248=ORIENTED_EDGE ( 'NONE', *, *, #545, .F. ) ;
#2262=FACE_OUTER_BOUND ( 'NONE', #5325, .T. ) ;
#2268=PRODUCT_CONTEXT ( 'NONE', #1516, 'mechanical' ) ;
#2283=ORIENTED_EDGE ( 'NONE', *, *, #2600, .F. ) ;
#2295=VECTOR ( 'NONE', #2788, 1000.000000000000000 ) ;
#2301=EDGE_LOOP ( 'NONE', ( #7044, #3698 ) ) ;
#2351=DIRECTION ( 'NONE',  ( 1.000000000000000000, 0.000000000000000000, 0.000000000000000000 ) ) ;
#2407=EDGE_CURVE ( 'NONE', #3577, #3835, #2752, .T. ) ;
#2465=ORIENTED_EDGE ( 'NONE', *, *, #6346, .F. ) ;
#2468=DIRECTION ( 'NONE',  ( 1.000000000000000000, 0.000000000000000000, 0.000000000000000000 ) ) ;
#2600=EDGE_CURVE ( 'NONE', #260, #4272, #4489, .T. ) ;
#2623=EDGE_CURVE ( 'NONE', #3835, #6817, #2880, .T. ) ;
#2635=EDGE_CURVE ( 'NONE', #387, #389, #5438, .T. ) ;
#2672=( GEOMETRIC_REPRESENTATION_CONTEXT ( 3 ) GLOBAL_UNCERTAINTY_ASSIGNED_CONTEXT ( ( #5606 ) ) GLOBAL_UNIT_ASSIGNED_CONTEXT ( ( #4459, #4541, #5022 ) ) REPRESENTATION_CONTEXT ( 'NONE', 'WORKASPACE' ) );
#2683=ADVANCED_BREP_SHAPE_REPRESENTATION ( '', ( #7024, #5785 ), #2702 ) ;
#2702=( GEOMETRIC_REPRESENTATION_CONTEXT ( 3 ) GLOBAL_UNCERTAINTY_ASSIGNED_CONTEXT ( ( #937 ) ) GLOBAL_UNIT_ASSIGNED_CONTEXT ( ( #5795, #7591, #3345 ) ) REPRESENTATION_CONTEXT ( 'NONE', 'WORKASPACE' ) );
#2752=CIRCLE ( 'NONE', #1461, 5.000000000000000888 ) ;
#2781=PLANE ( 'NONE',  #5430 ) ;
#2788=DIRECTION ( 'NONE',  ( -0.000000000000000000, -0.000000000000000000, -1.000000000000000000 ) ) ;
#2832=ADVANCED_FACE ( 'NONE', ( #1833 ), #3696, .T. ) ;
#2868=EDGE_LOOP ( 'NONE', ( #2031, #7809 ) ) ;
#2880=CIRCLE ( 'NONE', #7748, 12.50000000000000355 ) ;
#2939=ADVANCED_FACE ( 'NONE', ( #677 ), #4793, .T. ) ;
#2968=ORIENTED_EDGE ( 'NONE', *, *, #6346, .T. ) ;
#2982=CARTESIAN_POINT ( 'NONE',  ( 0.000000000000000000, 0.000000000000000000, 97.50000000000000000 ) ) ;
#2995=EDGE_LOOP ( 'NONE', ( #3317, #5151, #7053, #3614 ) ) ;
#3002=EDGE_LOOP ( 'NONE', ( #6120, #5755, #1280, #6389 ) ) ;
#3022=CARTESIAN_POINT ( 'NONE',  ( 0.000000000000000000, 0.000000000000000000, 2.500000000000085265 ) ) ;
#3026=CARTESIAN_POINT ( 'NONE',  ( -12.50000000000000000, 0.000000000000000000, 90.00000000000000000 ) ) ;
#3065=DIRECTION ( 'NONE',  ( 0.000000000000000000, 0.000000000000000000, 1.000000000000000000 ) ) ;
#3069=AXIS2_PLACEMENT_3D ( 'NONE', #4501, #1453, #5756 ) ;
#3070=CONICAL_SURFACE ( 'NONE', #6136, 12.50000000000000000, 0.7853981633974521648 ) ;
#3143=ADVANCED_FACE ( 'NONE', ( #5928 ), #5830, .T. ) ;
#3190=VECTOR ( 'NONE', #6594, 1000.000000000000000 ) ;
#3221=PRODUCT ( 'Bolt3', 'Bolt3', '', ( #2268 ) ) ;
#3227=EDGE_LOOP ( 'NONE', ( #4080, #5337, #7788, #4138 ) ) ;
#3317=ORIENTED_EDGE ( 'NONE', *, *, #7315, .F. ) ;
#3322=CARTESIAN_POINT ( 'NONE',  ( 0.000000000000000000, 0.000000000000000000, 97.50000000000000000 ) ) ;
#3336=DIRECTION ( 'NONE',  ( 1.000000000000000000, 0.000000000000000000, 0.000000000000000000 ) ) ;
#3345=( NAMED_UNIT ( * ) SI_UNIT ( $, .STERADIAN. ) SOLID_ANGLE_UNIT ( ) );
#3352=ORIENTED_EDGE ( 'NONE', *, *, #7315, .T. ) ;
#3353=PRODUCT_DEFINITION_CONTEXT ( 'detailed design', #6846, 'design' ) ;
#3454=CIRCLE ( 'NONE', #513, 17.50000000000000355 ) ;
#3459=DIRECTION ( 'NONE',  ( 0.000000000000000000, 0.000000000000000000, 1.000000000000000000 ) ) ;
#3465=DIRECTION ( 'NONE',  ( 1.000000000000000000, 0.000000000000000000, 0.000000000000000000 ) ) ;
#3496=EDGE_CURVE ( 'NONE', #6926, #6174, #4163, .T. ) ;
#3503=CARTESIAN_POINT ( 'NONE',  ( 0.000000000000000000, 0.000000000000000000, 2.500000000000085265 ) ) ;
#3562=EDGE_CURVE ( 'NONE', #5728, #6174, #6068, .T. ) ;
#3577=VERTEX_POINT ( 'NONE', #7139 ) ;
#3579=DIRECTION ( 'NONE',  ( -0.000000000000000000, -0.000000000000000000, -1.000000000000000000 ) ) ;
#3614=ORIENTED_EDGE ( 'NONE', *, *, #5118, .F. ) ;
#3623=DIRECTION ( 'NONE',  ( 1.000000000000000000, 0.000000000000000000, 0.000000000000000000 ) ) ;
#3696=CYLINDRICAL_SURFACE ( 'NONE', #2104, 12.50000000000000000 ) ;
#3698=ORIENTED_EDGE ( 'NONE', *, *, #2623, .T. ) ;
#3748=DIRECTION ( 'NONE',  ( -1.000000000000000000, 1.224646799147353454E-16, 0.000000000000000000 ) ) ;
#3818=CIRCLE ( 'NONE', #6639, 12.50000000000000355 ) ;
#3835=VERTEX_POINT ( 'NONE', #1314 ) ;
#3895=DIRECTION ( 'NONE',  ( 1.000000000000000000, 0.000000000000000000, 0.000000000000000000 ) ) ;
#3897=DIRECTION ( 'NONE',  ( 1.000000000000000000, 0.000000000000000000, -0.000000000000000000 ) ) ;
#3934=AXIS2_PLACEMENT_3D ( 'NONE', #3022, #5339, #7310 ) ;
#3960=CIRCLE ( 'NONE', #5758, 17.50000000000000355 ) ;
#3996=AXIS2_PLACEMENT_3D ( 'NONE', #5943, #6627, #6030 ) ;
#4080=ORIENTED_EDGE ( 'NONE', *, *, #5584, .F. ) ;
#4110=CARTESIAN_POINT ( 'NONE',  ( 0.000000000000000000, 0.000000000000000000, 0.000000000000000000 ) ) ;
#4138=ORIENTED_EDGE ( 'NONE', *, *, #4792, .T. ) ;
#4139=LINE ( 'NONE', #1664, #3190 ) ;
#4146=EDGE_LOOP ( 'NONE', ( #2283, #7808, #1284, #918 ) ) ;
#4163=CIRCLE ( 'NONE', #5314, 12.50000000000000000 ) ;
#4170=FACE_OUTER_BOUND ( 'NONE', #4146, .T. ) ;
#4186=DIRECTION ( 'NONE',  ( 0.000000000000000000, 0.000000000000000000, 1.000000000000000000 ) ) ;
#4191=CARTESIAN_POINT ( 'NONE',  ( 0.000000000000000000, 0.000000000000000000, 90.00000000000000000 ) ) ;
#4223=DIRECTION ( 'NONE',  ( -0.000000000000000000, -0.000000000000000000, -1.000000000000000000 ) ) ;
#4271=CLOSED_SHELL ( 'NONE', ( #2939, #3143, #24, #644, #2832, #2136, #6166, #4676, #1898, #4587, #6081 ) ) ;
#4272=VERTEX_POINT ( 'NONE', #1498 ) ;
#4300=DIRECTION ( 'NONE',  ( -1.000000000000000000, 0.000000000000000000, 0.000000000000000000 ) ) ;
#4301=FACE_OUTER_BOUND ( 'NONE', #2204, .T. ) ;
#4314=AXIS2_PLACEMENT_3D ( 'NONE', #2087, #4646, #7109 ) ;
#4329=DIRECTION ( 'NONE',  ( 1.224646799147353207E-16, 1.000000000000000000, -0.000000000000000000 ) ) ;
#4335=CIRCLE ( 'NONE', #7418, 17.50000000000000355 ) ;
#4358=CARTESIAN_POINT ( 'NONE',  ( 0.000000000000000000, 0.000000000000000000, 2.500000000000085265 ) ) ;
#4390=AXIS2_PLACEMENT_3D ( 'NONE', #6793, #6915, #3897 ) ;
#4459=( LENGTH_UNIT ( ) NAMED_UNIT ( * ) SI_UNIT ( .MILLI., .METRE. ) );
#4489=LINE ( 'NONE', #4607, #2102 ) ;
#4501=CARTESIAN_POINT ( 'NONE',  ( 0.000000000000000000, 0.000000000000000000, 90.00000000000000000 ) ) ;
#4541=( NAMED_UNIT ( * ) PLANE_ANGLE_UNIT ( ) SI_UNIT ( $, .RADIAN. ) );
#4552=EDGE_LOOP ( 'NONE', ( #3352, #4716, #2968, #2248 ) ) ;
#4565=DIRECTION ( 'NONE',  ( -0.000000000000000000, -0.000000000000000000, -1.000000000000000000 ) ) ;
#4569=FACE_OUTER_BOUND ( 'NONE', #1944, .T. ) ;
#4577=EDGE_CURVE ( 'NONE', #389, #6926, #5709, .T. ) ;
#4587=ADVANCED_FACE ( 'NONE', ( #4569 ), #5205, .T. ) ;
#4597=AXIS2_PLACEMENT_3D ( 'NONE', #2982, #3579, #5905 ) ;
#4607=CARTESIAN_POINT ( 'NONE',  ( 17.50000000000000355, 2.143131898507868643E-15, 97.50000000000000000 ) ) ;
#4646=DIRECTION ( 'NONE',  ( 0.000000000000000000, 0.000000000000000000, 1.000000000000000000 ) ) ;
#4670=DIRECTION ( 'NONE',  ( 1.000000000000000000, 0.000000000000000000, 0.000000000000000000 ) ) ;
#4676=ADVANCED_FACE ( 'NONE', ( #411 ), #6383, .T. ) ;
#4693=CARTESIAN_POINT ( 'NONE',  ( 0.000000000000000000, 0.000000000000000000, 0.000000000000000000 ) ) ;
#4697=VERTEX_POINT ( 'NONE', #1012 ) ;
#4716=ORIENTED_EDGE ( 'NONE', *, *, #2600, .T. ) ;
#4792=EDGE_CURVE ( 'NONE', #6174, #6926, #492, .T. ) ;
#4793=CONICAL_SURFACE ( 'NONE', #452, 12.50000000000000000, 0.7853981633974521648 ) ;
#4930=ORIENTED_EDGE ( 'NONE', *, *, #4577, .F. ) ;
#4962=DIRECTION ( 'NONE',  ( -1.000000000000000000, 0.000000000000000000, 0.000000000000000000 ) ) ;
#4987=FACE_OUTER_BOUND ( 'NONE', #7307, .T. ) ;
#5017=DIRECTION ( 'NONE',  ( -0.000000000000000000, -0.000000000000000000, -1.000000000000000000 ) ) ;
#5022=( NAMED_UNIT ( * ) SI_UNIT ( $, .STERADIAN. ) SOLID_ANGLE_UNIT ( ) );
#5033=ORIENTED_EDGE ( 'NONE', *, *, #3496, .T. ) ;
#5064=CARTESIAN_POINT ( 'NONE',  ( 12.50000000000000000, 1.530808498934191127E-15, 90.00000000000000000 ) ) ;
#5085=CARTESIAN_POINT ( 'NONE',  ( 12.50000000000000355, 0.000000000000000000, 92.50000000000000000 ) ) ;
#5118=EDGE_CURVE ( 'NONE', #260, #6817, #5861, .T. ) ;
#5122=ORIENTED_EDGE ( 'NONE', *, *, #2623, .F. ) ;
#5151=ORIENTED_EDGE ( 'NONE', *, *, #2407, .T. ) ;
#5170=DIRECTION ( 'NONE',  ( 0.000000000000000000, 0.000000000000000000, 1.000000000000000000 ) ) ;
#5204=CARTESIAN_POINT ( 'NONE',  ( 0.000000000000000000, 0.000000000000000000, 0.000000000000000000 ) ) ;
#5205=TOROIDAL_SURFACE ( 'NONE', #6758, 12.50000000000000355, 5.000000000000000000 ) ;
#5209=CARTESIAN_POINT ( 'NONE',  ( 0.000000000000000000, 0.000000000000000000, 2.500000000000085265 ) ) ;
#5220=MECHANICAL_DESIGN_GEOMETRIC_PRESENTATION_REPRESENTATION('',(#7660),#2672);
#5222=LINE ( 'NONE', #5064, #2295 ) ;
#5252=DIRECTION ( 'NONE',  ( 0.000000000000000000, 0.000000000000000000, 1.000000000000000000 ) ) ;
#5265=LINE ( 'NONE', #1179, #7230 ) ;
#5277=DIRECTION ( 'NONE',  ( -1.000000000000000000, 0.000000000000000000, 0.000000000000000000 ) ) ;
#5314=AXIS2_PLACEMENT_3D ( 'NONE', #3503, #7755, #6467 ) ;
#5325=EDGE_LOOP ( 'NONE', ( #1869, #1988 ) ) ;
#5337=ORIENTED_EDGE ( 'NONE', *, *, #127, .F. ) ;
#5339=DIRECTION ( 'NONE',  ( -0.000000000000000000, -0.000000000000000000, 1.000000000000000000 ) ) ;
#5412=EDGE_CURVE ( 'NONE', #6817, #3835, #3818, .T. ) ;
#5415=CARTESIAN_POINT ( 'NONE',  ( -12.50000000000000000, 0.000000000000000000, 2.500000000000085265 ) ) ;
#5425=CARTESIAN_POINT ( 'NONE',  ( 12.50000000000000000, 1.530808498934191127E-15, 90.00000000000000000 ) ) ;
#5430=AXIS2_PLACEMENT_3D ( 'NONE', #4693, #5170, #7625 ) ;
#5438=CIRCLE ( 'NONE', #1970, 9.999999999999896971 ) ;
#5465=DIRECTION ( 'NONE',  ( -0.000000000000000000, -0.000000000000000000, -1.000000000000000000 ) ) ;
#5493=CARTESIAN_POINT ( 'NONE',  ( 12.50000000000000355, 0.000000000000000000, 97.50000000000000000 ) ) ;
#5535=ORIENTED_EDGE ( 'NONE', *, *, #5118, .T. ) ;
#5584=EDGE_CURVE ( 'NONE', #5686, #6926, #5222, .T. ) ;
#5606=UNCERTAINTY_MEASURE_WITH_UNIT (LENGTH_MEASURE( 1.000000000000000082E-05 ), #4459, 'distance_accuracy_value', 'NONE');
#5625=CARTESIAN_POINT ( 'NONE',  ( 0.000000000000000000, 0.000000000000000000, 90.00000000000000000 ) ) ;
#5686=VERTEX_POINT ( 'NONE', #5425 ) ;
#5709=LINE ( 'NONE', #206, #5734 ) ;
#5722=CARTESIAN_POINT ( 'NONE',  ( 9.999999999999896971, 0.000000000000000000, 0.000000000000000000 ) ) ;
#5728=VERTEX_POINT ( 'NONE', #543 ) ;
#5734=VECTOR ( 'NONE', #46, 1000.000000000000000 ) ;
#5755=ORIENTED_EDGE ( 'NONE', *, *, #735, .F. ) ;
#5756=DIRECTION ( 'NONE',  ( 1.000000000000000000, 0.000000000000000000, 0.000000000000000000 ) ) ;
#5758=AXIS2_PLACEMENT_3D ( 'NONE', #6510, #1013, #3465 ) ;
#5785=AXIS2_PLACEMENT_3D ( 'NONE', #4110, #4186, #2351 ) ;
#5795=( LENGTH_UNIT ( ) NAMED_UNIT ( * ) SI_UNIT ( .MILLI., .METRE. ) );
#5812=CIRCLE ( 'NONE', #2230, 12.50000000000000000 ) ;
#5822=EDGE_CURVE ( 'NONE', #387, #6174, #4139, .T. ) ;
#5830=TOROIDAL_SURFACE ( 'NONE', #6341, 12.50000000000000355, 5.000000000000000000 ) ;
#5861=CIRCLE ( 'NONE', #7149, 5.000000000000004441 ) ;
#5905=DIRECTION ( 'NONE',  ( -1.000000000000000000, 0.000000000000000000, 0.000000000000000000 ) ) ;
#5928=FACE_OUTER_BOUND ( 'NONE', #2995, .T. ) ;
#5943=CARTESIAN_POINT ( 'NONE',  ( 0.000000000000000000, 0.000000000000000000, 90.00000000000000000 ) ) ;
#6030=DIRECTION ( 'NONE',  ( 1.000000000000000000, 0.000000000000000000, 0.000000000000000000 ) ) ;
#6068=LINE ( 'NONE', #3026, #7875 ) ;
#6081=ADVANCED_FACE ( 'NONE', ( #1411 ), #3070, .T. ) ;
#6116=DIRECTION ( 'NONE',  ( 1.000000000000000000, 0.000000000000000000, 0.000000000000000000 ) ) ;
#6120=ORIENTED_EDGE ( 'NONE', *, *, #5822, .F. ) ;
#6136=AXIS2_PLACEMENT_3D ( 'NONE', #5209, #2088, #3895 ) ;
#6166=ADVANCED_FACE ( 'NONE', ( #4170 ), #1127, .T. ) ;
#6174=VERTEX_POINT ( 'NONE', #5415 ) ;
#6184=CIRCLE ( 'NONE', #3996, 17.50000000000000355 ) ;
#6261=EDGE_CURVE ( 'NONE', #260, #3577, #3960, .T. ) ;
#6288=CARTESIAN_POINT ( 'NONE',  ( 12.50000000000000000, 1.530808498934191127E-15, 2.500000000000085265 ) ) ;
#6335=DIRECTION ( 'NONE',  ( 0.000000000000000000, -1.000000000000000000, 0.000000000000000000 ) ) ;
#6341=AXIS2_PLACEMENT_3D ( 'NONE', #394, #1153, #7882 ) ;
#6346=EDGE_CURVE ( 'NONE', #4272, #4697, #3454, .T. ) ;
#6383=PLANE ( 'NONE',  #4314 ) ;
#6389=ORIENTED_EDGE ( 'NONE', *, *, #4792, .F. ) ;
#6467=DIRECTION ( 'NONE',  ( 1.000000000000000000, 0.000000000000000000, 0.000000000000000000 ) ) ;
#6491=PRODUCT_DEFINITION_SHAPE ( 'NONE', 'NONE',  #1538 ) ;
#6503=CARTESIAN_POINT ( 'NONE',  ( 0.000000000000000000, 0.000000000000000000, 97.50000000000000000 ) ) ;
#6510=CARTESIAN_POINT ( 'NONE',  ( 0.000000000000000000, 0.000000000000000000, 92.50000000000000000 ) ) ;
#6554=PRODUCT_DEFINITION_FORMATION_WITH_SPECIFIED_SOURCE ( 'ANY', '', #3221, .NOT_KNOWN. ) ;
#6594=DIRECTION ( 'NONE',  ( -0.7071067811865502373, 8.659560562354966138E-17, 0.7071067811865447972 ) ) ;
#6627=DIRECTION ( 'NONE',  ( 0.000000000000000000, 0.000000000000000000, 1.000000000000000000 ) ) ;
#6639=AXIS2_PLACEMENT_3D ( 'NONE', #1978, #6837, #2468 ) ;
#6710=CARTESIAN_POINT ( 'NONE',  ( 0.000000000000000000, 0.000000000000000000, 0.000000000000000000 ) ) ;
#6733=DIRECTION ( 'NONE',  ( -0.000000000000000000, -0.000000000000000000, -1.000000000000000000 ) ) ;
#6758=AXIS2_PLACEMENT_3D ( 'NONE', #969, #5252, #1532 ) ;
#6792=CYLINDRICAL_SURFACE ( 'NONE', #2246, 12.50000000000000000 ) ;
#6793=CARTESIAN_POINT ( 'NONE',  ( 0.000000000000000000, 0.000000000000000000, 90.00000000000000000 ) ) ;
#6815=DIRECTION ( 'NONE',  ( -0.000000000000000000, -0.000000000000000000, 1.000000000000000000 ) ) ;
#6817=VERTEX_POINT ( 'NONE', #5493 ) ;
#6829=CARTESIAN_POINT ( 'NONE',  ( 0.000000000000000000, 0.000000000000000000, 90.00000000000000000 ) ) ;
#6837=DIRECTION ( 'NONE',  ( 0.000000000000000000, 0.000000000000000000, 1.000000000000000000 ) ) ;
#6838=CARTESIAN_POINT ( 'NONE',  ( 17.50000000000000355, 2.143131898507868643E-15, 92.50000000000000000 ) ) ;
#6846=APPLICATION_CONTEXT ( 'automotive_design' ) ;
#6860=ORIENTED_EDGE ( 'NONE', *, *, #3496, .F. ) ;
#6910=SHAPE_REPRESENTATION ( 'Bolt3', ( #5785 ), #2702 ) ;
#6915=DIRECTION ( 'NONE',  ( 0.000000000000000000, 0.000000000000000000, 1.000000000000000000 ) ) ;
#6926=VERTEX_POINT ( 'NONE', #6288 ) ;
#6943=ORIENTED_EDGE ( 'NONE', *, *, #2635, .F. ) ;
#6967=DIRECTION ( 'NONE',  ( -0.000000000000000000, -0.000000000000000000, -1.000000000000000000 ) ) ;
#6996=ORIENTED_EDGE ( 'NONE', *, *, #5584, .T. ) ;
#7024=MANIFOLD_SOLID_BREP ( 'Pah1', #4271 ) ;
#7044=ORIENTED_EDGE ( 'NONE', *, *, #5412, .T. ) ;
#7045=EDGE_CURVE ( 'NONE', #5686, #5728, #2026, .T. ) ;
#7053=ORIENTED_EDGE ( 'NONE', *, *, #5412, .F. ) ;
#7109=DIRECTION ( 'NONE',  ( 1.000000000000000000, 0.000000000000000000, -0.000000000000000000 ) ) ;
#7139=CARTESIAN_POINT ( 'NONE',  ( -17.50000000000000355, 0.000000000000000000, 92.50000000000000000 ) ) ;
#7149=AXIS2_PLACEMENT_3D ( 'NONE', #5085, #6335, #7502 ) ;
#7230=VECTOR ( 'NONE', #4223, 1000.000000000000000 ) ;
#7254=DIRECTION ( 'NONE',  ( 0.000000000000000000, 0.000000000000000000, 1.000000000000000000 ) ) ;
#7307=EDGE_LOOP ( 'NONE', ( #514, #6996, #5033, #7695 ) ) ;
#7310=DIRECTION ( 'NONE',  ( 1.000000000000000000, 0.000000000000000000, 0.000000000000000000 ) ) ;
#7315=EDGE_CURVE ( 'NONE', #3577, #260, #4335, .T. ) ;
#7418=AXIS2_PLACEMENT_3D ( 'NONE', #1133, #7905, #3623 ) ;
#7494=CARTESIAN_POINT ( 'NONE',  ( 0.000000000000000000, 0.000000000000000000, 90.00000000000000000 ) ) ;
#7502=DIRECTION ( 'NONE',  ( 0.000000000000000000, 0.000000000000000000, -1.000000000000000000 ) ) ;
#7591=( NAMED_UNIT ( * ) PLANE_ANGLE_UNIT ( ) SI_UNIT ( $, .RADIAN. ) );
#7614=ORIENTED_EDGE ( 'NONE', *, *, #1103, .F. ) ;
#7625=DIRECTION ( 'NONE',  ( 1.000000000000000000, 0.000000000000000000, -0.000000000000000000 ) ) ;
#7660=STYLED_ITEM('',(#7969),#7024);
#7695=ORIENTED_EDGE ( 'NONE', *, *, #3562, .F. ) ;
#7735=AXIS2_PLACEMENT_3D ( 'NONE', #3322, #6967, #5277 ) ;
#7748=AXIS2_PLACEMENT_3D ( 'NONE', #6503, #3459, #2083 ) ;
#7755=DIRECTION ( 'NONE',  ( -0.000000000000000000, -0.000000000000000000, 1.000000000000000000 ) ) ;
#7788=ORIENTED_EDGE ( 'NONE', *, *, #3562, .T. ) ;
#7808=ORIENTED_EDGE ( 'NONE', *, *, #6261, .T. ) ;
#7809=ORIENTED_EDGE ( 'NONE', *, *, #7045, .T. ) ;
#7871=ORIENTED_EDGE ( 'NONE', *, *, #6261, .F. ) ;
#7875=VECTOR ( 'NONE', #5465, 1000.000000000000000 ) ;
#7882=DIRECTION ( 'NONE',  ( 1.000000000000000000, 0.000000000000000000, 0.000000000000000000 ) ) ;
#7905=DIRECTION ( 'NONE',  ( -0.000000000000000000, -0.000000000000000000, -1.000000000000000000 ) ) ;
#7963=COLOUR_RGB('Black',0.12,0.14,0.17);
#7964=FILL_AREA_STYLE_COLOUR('',#7963);
#7965=FILL_AREA_STYLE('',(#7964));
#7966=SURFACE_STYLE_FILL_AREA(#7965);
#7967=SURFACE_SIDE_STYLE('',(#7966));
#7968=SURFACE_STYLE_USAGE(.BOTH.,#7967);
#7969=PRESENTATION_STYLE_ASSIGNMENT((#7968));
ENDSEC;
END-ISO-10303-21;
